ISO-10303-21;
HEADER;
FILE_DESCRIPTION (('STEP AP203'),
    '1' );
FILE_NAME ('BladeScrew_Predeterminado.step',
    '2026-10-08T11:28:20',
    ( '' ),
    ( '' ),
    'SwSTEP 2.0',
    'SolidWorks 2024',
    '' );
FILE_SCHEMA (( 'AUTOMOTIVE_DESIGN' ));
ENDSEC;

DATA;
#2=DIRECTION ( 'NONE',  ( 0.000000000000000000, 0.000000000000000000, -1.000000000000000000 ) ) ;
#41=DIRECTION ( 'NONE',  ( -0.000000000000000000, -1.000000000000000000, -0.000000000000000000 ) ) ;
#45=EDGE_CURVE ( 'NONE', #5739, #9776, #9697, .T. ) ;
#60=FACE_OUTER_BOUND ( 'NONE', #10831, .T. ) ;
#71=AXIS2_PLACEMENT_3D ( 'NONE', #14775, #7400, #12125 ) ;
#102=ORIENTED_EDGE ( 'NONE', *, *, #10097, .F. ) ;
#132=CARTESIAN_POINT ( 'NONE',  ( 0.000000000000000000, 0.000000000000000000, -2.000000000000000000 ) ) ;
#259=AXIS2_PLACEMENT_3D ( 'NONE', #6513, #5353, #11151 ) ;
#323=DIRECTION ( 'NONE',  ( 0.000000000000000000, 0.000000000000000000, -1.000000000000000000 ) ) ;
#325=ORIENTED_EDGE ( 'NONE', *, *, #7627, .F. ) ;
#347=CARTESIAN_POINT ( 'NONE',  ( -0.2500000000000000555, 5.000000000000000000, -0.2499999999999997780 ) ) ;
#372=VECTOR ( 'NONE', #723, 1000.000000000000000 ) ;
#398=CARTESIAN_POINT ( 'NONE',  ( -0.2500000000000000555, 4.500000000000000888, 1.500000000000000222 ) ) ;
#472=DIRECTION ( 'NONE',  ( 0.000000000000000000, 0.000000000000000000, 1.000000000000000000 ) ) ;
#494=CARTESIAN_POINT ( 'NONE',  ( 0.000000000000000000, 5.000000000000000000, 0.000000000000000000 ) ) ;
#496=VECTOR ( 'NONE', #13337, 1000.000000000000000 ) ;
#521=EDGE_LOOP ( 'NONE', ( #12296, #11775, #1028, #6715 ) ) ;
#537=VECTOR ( 'NONE', #8626, 1000.000000000000000 ) ;
#589=CARTESIAN_POINT ( 'NONE',  ( -1.500000000000000000, 4.500000000000000888, -0.2499999999999997780 ) ) ;
#643=ADVANCED_FACE ( 'NONE', ( #2562 ), #1239, .T. ) ;
#646=FACE_OUTER_BOUND ( 'NONE', #14205, .T. ) ;
#687=CARTESIAN_POINT ( 'NONE',  ( 0.000000000000000000, 4.000000000000000000, 0.000000000000000000 ) ) ;
#723=DIRECTION ( 'NONE',  ( 0.000000000000000000, 0.000000000000000000, -1.000000000000000000 ) ) ;
#727=ORIENTED_EDGE ( 'NONE', *, *, #12802, .F. ) ;
#749=EDGE_CURVE ( 'NONE', #14051, #14170, #2686, .T. ) ;
#876=DIRECTION ( 'NONE',  ( -0.000000000000000000, -1.000000000000000000, -0.000000000000000000 ) ) ;
#897=ORIENTED_EDGE ( 'NONE', *, *, #10097, .T. ) ;
#901=ORIENTED_EDGE ( 'NONE', *, *, #12261, .F. ) ;
#914=VERTEX_POINT ( 'NONE', #12365 ) ;
#1025=DIRECTION ( 'NONE',  ( 1.000000000000000000, 0.000000000000000000, 0.000000000000000000 ) ) ;
#1028=ORIENTED_EDGE ( 'NONE', *, *, #10486, .T. ) ;
#1042=PLANE ( 'NONE',  #8379 ) ;
#1086=DIRECTION ( 'NONE',  ( 1.000000000000000000, 0.000000000000000000, 0.000000000000000000 ) ) ;
#1094=CARTESIAN_POINT ( 'NONE',  ( -1.500000000000000000, 4.500000000000000888, -0.2499999999999997780 ) ) ;
#1113=EDGE_CURVE ( 'NONE', #9776, #13724, #15007, .T. ) ;
#1123=ORIENTED_EDGE ( 'NONE', *, *, #12013, .T. ) ;
#1237=DIRECTION ( 'NONE',  ( -0.000000000000000000, 0.000000000000000000, 1.000000000000000000 ) ) ;
#1239=PLANE ( 'NONE',  #12508 ) ;
#1270=VECTOR ( 'NONE', #8112, 1000.000000000000000 ) ;
#1271=ORIENTED_EDGE ( 'NONE', *, *, #2692, .F. ) ;
#1273=CARTESIAN_POINT ( 'NONE',  ( 0.000000000000000000, 5.000000000000000000, 0.000000000000000000 ) ) ;
#1301=LINE ( 'NONE', #14461, #11856 ) ;
#1308=VERTEX_POINT ( 'NONE', #7081 ) ;
#1330=ORIENTED_EDGE ( 'NONE', *, *, #749, .F. ) ;
#1341=DIRECTION ( 'NONE',  ( 1.000000000000000000, 0.000000000000000000, 0.000000000000000000 ) ) ;
#1348=ORIENTED_EDGE ( 'NONE', *, *, #12802, .T. ) ;
#1350=DIRECTION ( 'NONE',  ( -0.000000000000000000, 1.000000000000000000, -0.000000000000000000 ) ) ;
#1353=CYLINDRICAL_SURFACE ( 'NONE', #4541, 3.500000000000000000 ) ;
#1366=ADVANCED_FACE ( 'NONE', ( #9731 ), #1453, .F. ) ;
#1397=CARTESIAN_POINT ( 'NONE',  ( 0.000000000000000000, 4.000000000000000000, 0.000000000000000000 ) ) ;
#1400=EDGE_CURVE ( 'NONE', #5040, #11885, #1301, .T. ) ;
#1428=ORIENTED_EDGE ( 'NONE', *, *, #6458, .F. ) ;
#1453=PLANE ( 'NONE',  #14090 ) ;
#1486=EDGE_LOOP ( 'NONE', ( #897, #6728, #13316, #1428 ) ) ;
#1488=EDGE_CURVE ( 'NONE', #7451, #3391, #6082, .T. ) ;
#1513=DIRECTION ( 'NONE',  ( 0.000000000000000000, 1.000000000000000000, 0.000000000000000000 ) ) ;
#1529=CARTESIAN_POINT ( 'NONE',  ( -0.2500000000000000555, 5.000000000000000000, -1.499999999999999778 ) ) ;
#1585=EDGE_LOOP ( 'NONE', ( #9449, #3500 ) ) ;
#1609=LINE ( 'NONE', #13208, #537 ) ;
#1683=EDGE_CURVE ( 'NONE', #6835, #914, #2487, .T. ) ;
#1686=EDGE_LOOP ( 'NONE', ( #14143, #6792, #4267, #8751 ) ) ;
#1699=CARTESIAN_POINT ( 'NONE',  ( 0.000000000000000000, 5.000000000000000000, 0.000000000000000000 ) ) ;
#1707=ORIENTED_EDGE ( 'NONE', *, *, #10438, .F. ) ;
#1725=LINE ( 'NONE', #8765, #10142 ) ;
#1729=VECTOR ( 'NONE', #14064, 1000.000000000000000 ) ;
#1740=FACE_OUTER_BOUND ( 'NONE', #8505, .T. ) ;
#1772=ADVANCED_FACE ( 'NONE', ( #11109 ), #8869, .T. ) ;
#1790=PLANE ( 'NONE',  #15147 ) ;
#1836=VECTOR ( 'NONE', #1086, 1000.000000000000000 ) ;
#1861=DIRECTION ( 'NONE',  ( 1.000000000000000000, 0.000000000000000000, 0.000000000000000000 ) ) ;
#1992=VECTOR ( 'NONE', #10708, 1000.000000000000000 ) ;
#2061=ORIENTED_EDGE ( 'NONE', *, *, #2523, .F. ) ;
#2092=ORIENTED_EDGE ( 'NONE', *, *, #6406, .T. ) ;
#2096=CARTESIAN_POINT ( 'NONE',  ( 0.2499999999999999445, 4.500000000000000888, -1.499999999999999778 ) ) ;
#2269=DIRECTION ( 'NONE',  ( 0.000000000000000000, 1.000000000000000000, 0.000000000000000000 ) ) ;
#2312=CARTESIAN_POINT ( 'NONE',  ( -1.500000000000000000, 5.000000000000000000, 0.2500000000000002220 ) ) ;
#2341=ORIENTED_EDGE ( 'NONE', *, *, #14255, .F. ) ;
#2346=CARTESIAN_POINT ( 'NONE',  ( 0.000000000000000000, 0.000000000000000000, 0.000000000000000000 ) ) ;
#2360=ORIENTED_EDGE ( 'NONE', *, *, #13576, .T. ) ;
#2392=CLOSED_SHELL ( 'NONE', ( #6961, #2606, #9238, #9817, #10544, #4049, #1772, #14023, #6015, #5597, #643, #8244, #13312, #3294, #6173, #4241, #1366, #5743, #3178, #8056 ) ) ;
#2398=CARTESIAN_POINT ( 'NONE',  ( -0.2500000000000000555, 4.500000000000000888, -0.2499999999999997780 ) ) ;
#2466=ORIENTED_EDGE ( 'NONE', *, *, #7191, .F. ) ;
#2469=CARTESIAN_POINT ( 'NONE',  ( 0.000000000000000000, 0.000000000000000000, 0.000000000000000000 ) ) ;
#2480=DIRECTION ( 'NONE',  ( 0.000000000000000000, 0.000000000000000000, 1.000000000000000000 ) ) ;
#2487=CIRCLE ( 'NONE', #3465, 3.500000000000000000 ) ;
#2523=EDGE_CURVE ( 'NONE', #9024, #7289, #4899, .T. ) ;
#2541=DIRECTION ( 'NONE',  ( -0.000000000000000000, 0.000000000000000000, 1.000000000000000000 ) ) ;
#2562=FACE_OUTER_BOUND ( 'NONE', #12563, .T. ) ;
#2585=VERTEX_POINT ( 'NONE', #14428 ) ;
#2606=ADVANCED_FACE ( 'NONE', ( #13260 ), #13096, .T. ) ;
#2643=PRODUCT_DEFINITION_SHAPE ( 'NONE', 'NONE',  #9258 ) ;
#2665=CARTESIAN_POINT ( 'NONE',  ( 1.500000000000000000, 4.500000000000000888, -0.2499999999999997780 ) ) ;
#2673=PLANE ( 'NONE',  #10955 ) ;
#2686=CIRCLE ( 'NONE', #11805, 2.000000000000000000 ) ;
#2692=EDGE_CURVE ( 'NONE', #12952, #13724, #5360, .T. ) ;
#2767=VECTOR ( 'NONE', #6241, 1000.000000000000000 ) ;
#2806=CARTESIAN_POINT ( 'NONE',  ( 0.2499999999999999445, 4.500000000000000888, -0.2499999999999997780 ) ) ;
#2886=DIRECTION ( 'NONE',  ( 1.000000000000000000, 0.000000000000000000, 0.000000000000000000 ) ) ;
#2891=EDGE_CURVE ( 'NONE', #10548, #4391, #5215, .T. ) ;
#2902=ORIENTED_EDGE ( 'NONE', *, *, #14787, .T. ) ;
#2918=DIRECTION ( 'NONE',  ( 0.000000000000000000, 1.000000000000000000, 0.000000000000000000 ) ) ;
#2949=FACE_OUTER_BOUND ( 'NONE', #8077, .T. ) ;
#2974=EDGE_CURVE ( 'NONE', #14170, #6819, #5582, .T. ) ;
#3040=CARTESIAN_POINT ( 'NONE',  ( -1.500000000000000000, 4.500000000000000888, 0.2500000000000002220 ) ) ;
#3064=CARTESIAN_POINT ( 'NONE',  ( 4.286263797015736595E-16, 4.000000000000000000, 3.500000000000000000 ) ) ;
#3075=DIRECTION ( 'NONE',  ( 0.000000000000000000, 0.000000000000000000, -1.000000000000000000 ) ) ;
#3085=CARTESIAN_POINT ( 'NONE',  ( 1.500000000000000000, 4.500000000000000888, 0.2500000000000002220 ) ) ;
#3102=DIRECTION ( 'NONE',  ( 0.000000000000000000, -1.000000000000000000, 0.000000000000000000 ) ) ;
#3104=FACE_OUTER_BOUND ( 'NONE', #7924, .T. ) ;
#3131=CARTESIAN_POINT ( 'NONE',  ( 0.2499999999999999445, 5.000000000000000000, 0.2500000000000002220 ) ) ;
#3174=DIRECTION ( 'NONE',  ( 1.000000000000000000, 0.000000000000000000, 0.000000000000000000 ) ) ;
#3178=ADVANCED_FACE ( 'NONE', ( #14313 ), #14401, .F. ) ;
#3294=ADVANCED_FACE ( 'NONE', ( #5748 ), #1042, .T. ) ;
#3302=DIRECTION ( 'NONE',  ( 1.000000000000000000, 0.000000000000000000, 0.000000000000000000 ) ) ;
#3315=VECTOR ( 'NONE', #9535, 1000.000000000000000 ) ;
#3391=VERTEX_POINT ( 'NONE', #3131 ) ;
#3459=CARTESIAN_POINT ( 'NONE',  ( 0.000000000000000000, 4.000000000000000000, -2.000000000000000000 ) ) ;
#3465=AXIS2_PLACEMENT_3D ( 'NONE', #687, #14769, #5392 ) ;
#3500=ORIENTED_EDGE ( 'NONE', *, *, #9690, .F. ) ;
#3523=CARTESIAN_POINT ( 'NONE',  ( -1.500000000000000000, 4.500000000000000888, -0.2499999999999997780 ) ) ;
#3545=CIRCLE ( 'NONE', #13445, 3.500000000000000000 ) ;
#3580=CARTESIAN_POINT ( 'NONE',  ( 0.000000000000000000, 4.000000000000000000, 0.000000000000000000 ) ) ;
#3617=PRODUCT ( 'BladeScrew_Predeterminado', 'BladeScrew_Predeterminado', '', ( #6000 ) ) ;
#3628=DIRECTION ( 'NONE',  ( 0.000000000000000000, -0.000000000000000000, 1.000000000000000000 ) ) ;
#3662=ORIENTED_EDGE ( 'NONE', *, *, #10486, .F. ) ;
#3683=LINE ( 'NONE', #1529, #2767 ) ;
#3711=AXIS2_PLACEMENT_3D ( 'NONE', #9906, #11981, #323 ) ;
#3733=DIRECTION ( 'NONE',  ( 0.000000000000000000, 1.000000000000000000, 0.000000000000000000 ) ) ;
#3806=VECTOR ( 'NONE', #12680, 1000.000000000000000 ) ;
#3816=SHAPE_REPRESENTATION_RELATIONSHIP ( 'NONE' , 'NONE' ,  #12477, #14249 ) ;
#3818=VECTOR ( 'NONE', #876, 1000.000000000000000 ) ;
#3823=ORIENTED_EDGE ( 'NONE', *, *, #14188, .F. ) ;
#3857=DIRECTION ( 'NONE',  ( 0.000000000000000000, 0.000000000000000000, -1.000000000000000000 ) ) ;
#3869=EDGE_CURVE ( 'NONE', #5891, #7451, #4758, .T. ) ;
#3881=ORIENTED_EDGE ( 'NONE', *, *, #1683, .T. ) ;
#3884=ORIENTED_EDGE ( 'NONE', *, *, #12073, .F. ) ;
#3967=EDGE_LOOP ( 'NONE', ( #9214, #2902, #7394, #7372, #7939, #7158, #10529, #10261, #4608, #325, #10881, #13998 ) ) ;
#3984=CARTESIAN_POINT ( 'NONE',  ( -0.2500000000000000555, 4.500000000000000888, 1.500000000000000222 ) ) ;
#4000=AXIS2_PLACEMENT_3D ( 'NONE', #4274, #5499, #4196 ) ;
#4006=DIRECTION ( 'NONE',  ( 0.000000000000000000, 0.000000000000000000, 1.000000000000000000 ) ) ;
#4049=ADVANCED_FACE ( 'NONE', ( #8613, #13349 ), #11022, .F. ) ;
#4083=VECTOR ( 'NONE', #12466, 1000.000000000000000 ) ;
#4181=DIRECTION ( 'NONE',  ( 0.000000000000000000, 1.000000000000000000, 0.000000000000000000 ) ) ;
#4196=DIRECTION ( 'NONE',  ( 0.000000000000000000, 0.000000000000000000, -1.000000000000000000 ) ) ;
#4198=DIRECTION ( 'NONE',  ( 1.000000000000000000, 0.000000000000000000, 0.000000000000000000 ) ) ;
#4241=ADVANCED_FACE ( 'NONE', ( #4741 ), #13016, .F. ) ;
#4243=EDGE_CURVE ( 'NONE', #914, #6835, #14087, .T. ) ;
#4267=ORIENTED_EDGE ( 'NONE', *, *, #9690, .T. ) ;
#4274=CARTESIAN_POINT ( 'NONE',  ( 0.2499999999999999445, 4.500000000000000888, 1.500000000000000222 ) ) ;
#4292=EDGE_LOOP ( 'NONE', ( #12251, #1707, #5675, #102 ) ) ;
#4389=EDGE_CURVE ( 'NONE', #5529, #6819, #10372, .T. ) ;
#4391=VERTEX_POINT ( 'NONE', #7439 ) ;
#4425=CARTESIAN_POINT ( 'NONE',  ( -1.500000000000000000, 5.000000000000000000, 0.2500000000000002220 ) ) ;
#4466=AXIS2_PLACEMENT_3D ( 'NONE', #8947, #7629, #3075 ) ;
#4503=CARTESIAN_POINT ( 'NONE',  ( -1.500000000000000000, 5.000000000000000000, 0.2500000000000002220 ) ) ;
#4541=AXIS2_PLACEMENT_3D ( 'NONE', #1273, #41, #11632 ) ;
#4556=AXIS2_PLACEMENT_3D ( 'NONE', #494, #5212, #13493 ) ;
#4600=CARTESIAN_POINT ( 'NONE',  ( 0.2499999999999999445, 4.500000000000000888, 0.2500000000000002220 ) ) ;
#4602=ORIENTED_EDGE ( 'NONE', *, *, #12990, .T. ) ;
#4608=ORIENTED_EDGE ( 'NONE', *, *, #14188, .T. ) ;
#4643=CARTESIAN_POINT ( 'NONE',  ( -0.2500000000000000555, 5.000000000000000000, 1.500000000000000222 ) ) ;
#4653=ORIENTED_EDGE ( 'NONE', *, *, #6584, .F. ) ;
#4667=CARTESIAN_POINT ( 'NONE',  ( -0.2500000000000000555, 4.500000000000000888, 0.2500000000000002220 ) ) ;
#4716=AXIS2_PLACEMENT_3D ( 'NONE', #11870, #12254, #11089 ) ;
#4741=FACE_OUTER_BOUND ( 'NONE', #9613, .T. ) ;
#4758=LINE ( 'NONE', #6229, #1992 ) ;
#4774=SHAPE_DEFINITION_REPRESENTATION ( #2643, #12477 ) ;
#4777=CARTESIAN_POINT ( 'NONE',  ( 0.2499999999999999445, 5.000000000000000000, 1.500000000000000222 ) ) ;
#4866=LINE ( 'NONE', #2398, #1270 ) ;
#4871=CARTESIAN_POINT ( 'NONE',  ( 0.2499999999999999445, 4.500000000000000888, 1.500000000000000222 ) ) ;
#4899=LINE ( 'NONE', #2665, #11864 ) ;
#4927=CARTESIAN_POINT ( 'NONE',  ( -1.500000000000000000, 4.500000000000000888, 0.2500000000000002220 ) ) ;
#4949=VECTOR ( 'NONE', #1025, 1000.000000000000000 ) ;
#4999=ORIENTED_EDGE ( 'NONE', *, *, #5285, .T. ) ;
#5031=AXIS2_PLACEMENT_3D ( 'NONE', #1094, #1237, #10519 ) ;
#5040=VERTEX_POINT ( 'NONE', #398 ) ;
#5119=CARTESIAN_POINT ( 'NONE',  ( 1.500000000000000000, 4.500000000000000888, 0.2500000000000002220 ) ) ;
#5192=FACE_OUTER_BOUND ( 'NONE', #4292, .T. ) ;
#5212=DIRECTION ( 'NONE',  ( 0.000000000000000000, 1.000000000000000000, 0.000000000000000000 ) ) ;
#5215=LINE ( 'NONE', #14659, #496 ) ;
#5252=PLANE ( 'NONE',  #71 ) ;
#5263=EDGE_CURVE ( 'NONE', #5040, #5891, #9476, .T. ) ;
#5267=UNCERTAINTY_MEASURE_WITH_UNIT (LENGTH_MEASURE( 1.000000000000000082E-05 ), #6124, 'distance_accuracy_value', 'NONE');
#5285=EDGE_CURVE ( 'NONE', #2585, #14605, #10267, .T. ) ;
#5299=ORIENTED_EDGE ( 'NONE', *, *, #11781, .T. ) ;
#5353=DIRECTION ( 'NONE',  ( 0.000000000000000000, 1.000000000000000000, 0.000000000000000000 ) ) ;
#5360=LINE ( 'NONE', #12389, #10634 ) ;
#5363=CARTESIAN_POINT ( 'NONE',  ( -0.2500000000000000555, 5.000000000000000000, 1.500000000000000222 ) ) ;
#5383=ORIENTED_EDGE ( 'NONE', *, *, #12030, .T. ) ;
#5392=DIRECTION ( 'NONE',  ( 0.000000000000000000, 0.000000000000000000, 1.000000000000000000 ) ) ;
#5423=CARTESIAN_POINT ( 'NONE',  ( -1.500000000000000000, 4.500000000000000888, 0.2500000000000002220 ) ) ;
#5433=EDGE_LOOP ( 'NONE', ( #10752, #7466 ) ) ;
#5482=DIRECTION ( 'NONE',  ( -0.000000000000000000, 1.000000000000000000, -0.000000000000000000 ) ) ;
#5488=ORIENTED_EDGE ( 'NONE', *, *, #14414, .T. ) ;
#5499=DIRECTION ( 'NONE',  ( 1.000000000000000000, 0.000000000000000000, 0.000000000000000000 ) ) ;
#5529=VERTEX_POINT ( 'NONE', #132 ) ;
#5582=LINE ( 'NONE', #13864, #7646 ) ;
#5597=ADVANCED_FACE ( 'NONE', ( #60 ), #7146, .T. ) ;
#5607=ORIENTED_EDGE ( 'NONE', *, *, #12030, .F. ) ;
#5639=CARTESIAN_POINT ( 'NONE',  ( -0.2500000000000000555, 5.000000000000000000, 0.2500000000000002220 ) ) ;
#5675=ORIENTED_EDGE ( 'NONE', *, *, #5285, .F. ) ;
#5703=CARTESIAN_POINT ( 'NONE',  ( 0.2499999999999999445, 4.500000000000000888, -1.499999999999999778 ) ) ;
#5739=VERTEX_POINT ( 'NONE', #8847 ) ;
#5743=ADVANCED_FACE ( 'NONE', ( #1740 ), #12554, .T. ) ;
#5748=FACE_OUTER_BOUND ( 'NONE', #10800, .T. ) ;
#5761=CARTESIAN_POINT ( 'NONE',  ( 0.000000000000000000, 5.000000000000000000, -3.500000000000000000 ) ) ;
#5765=VECTOR ( 'NONE', #1861, 1000.000000000000000 ) ;
#5767=LINE ( 'NONE', #10326, #14633 ) ;
#5837=CARTESIAN_POINT ( 'NONE',  ( 1.500000000000000000, 5.000000000000000000, 0.2500000000000002220 ) ) ;
#5848=DIRECTION ( 'NONE',  ( -0.000000000000000000, -1.000000000000000000, -0.000000000000000000 ) ) ;
#5880=DIRECTION ( 'NONE',  ( 0.000000000000000000, 0.000000000000000000, 1.000000000000000000 ) ) ;
#5891=VERTEX_POINT ( 'NONE', #8285 ) ;
#5960=CARTESIAN_POINT ( 'NONE',  ( -1.500000000000000000, 4.500000000000000888, -0.2499999999999997780 ) ) ;
#5993=EDGE_CURVE ( 'NONE', #11845, #11885, #8828, .T. ) ;
#6000=MECHANICAL_CONTEXT ( 'NONE', #10340, 'mechanical' ) ;
#6009=EDGE_CURVE ( 'NONE', #12700, #9908, #8757, .T. ) ;
#6014=DIRECTION ( 'NONE',  ( 0.000000000000000000, 1.000000000000000000, 0.000000000000000000 ) ) ;
#6015=ADVANCED_FACE ( 'NONE', ( #646 ), #13488, .F. ) ;
#6068=CARTESIAN_POINT ( 'NONE',  ( 0.2499999999999999445, 4.500000000000000888, 0.2500000000000002220 ) ) ;
#6082=LINE ( 'NONE', #4777, #11367 ) ;
#6124=( LENGTH_UNIT ( ) NAMED_UNIT ( * ) SI_UNIT ( .MILLI., .METRE. ) );
#6128=LINE ( 'NONE', #10843, #3818 ) ;
#6136=LINE ( 'NONE', #6219, #11194 ) ;
#6173=ADVANCED_FACE ( 'NONE', ( #10290 ), #12842, .T. ) ;
#6198=LINE ( 'NONE', #5960, #12669 ) ;
#6219=CARTESIAN_POINT ( 'NONE',  ( -1.500000000000000000, 4.500000000000000888, 0.2500000000000002220 ) ) ;
#6224=DIRECTION ( 'NONE',  ( 0.000000000000000000, -0.000000000000000000, 1.000000000000000000 ) ) ;
#6228=( GEOMETRIC_REPRESENTATION_CONTEXT ( 3 ) GLOBAL_UNCERTAINTY_ASSIGNED_CONTEXT ( ( #5267 ) ) GLOBAL_UNIT_ASSIGNED_CONTEXT ( ( #6124, #14332, #7281 ) ) REPRESENTATION_CONTEXT ( 'NONE', 'WORKASPACE' ) );
#6229=CARTESIAN_POINT ( 'NONE',  ( 0.2499999999999999445, 4.500000000000000888, 1.500000000000000222 ) ) ;
#6239=AXIS2_PLACEMENT_3D ( 'NONE', #8789, #2918, #4006 ) ;
#6241=DIRECTION ( 'NONE',  ( 1.000000000000000000, 0.000000000000000000, 0.000000000000000000 ) ) ;
#6274=ORIENTED_EDGE ( 'NONE', *, *, #6009, .F. ) ;
#6356=ORIENTED_EDGE ( 'NONE', *, *, #6009, .T. ) ;
#6378=DIRECTION ( 'NONE',  ( 0.000000000000000000, 1.000000000000000000, 0.000000000000000000 ) ) ;
#6406=EDGE_CURVE ( 'NONE', #9158, #1308, #3545, .T. ) ;
#6423=CARTESIAN_POINT ( 'NONE',  ( -1.500000000000000000, 5.000000000000000000, 0.2500000000000002220 ) ) ;
#6440=CARTESIAN_POINT ( 'NONE',  ( 0.2499999999999999445, 4.500000000000000888, 1.500000000000000222 ) ) ;
#6458=EDGE_CURVE ( 'NONE', #10548, #7289, #11351, .T. ) ;
#6503=VERTEX_POINT ( 'NONE', #2312 ) ;
#6513=CARTESIAN_POINT ( 'NONE',  ( 0.000000000000000000, 0.000000000000000000, 0.000000000000000000 ) ) ;
#6584=EDGE_CURVE ( 'NONE', #9158, #914, #15237, .T. ) ;
#6598=ORIENTED_EDGE ( 'NONE', *, *, #5263, .F. ) ;
#6715=ORIENTED_EDGE ( 'NONE', *, *, #10438, .T. ) ;
#6722=CARTESIAN_POINT ( 'NONE',  ( -0.2500000000000000555, 4.500000000000000888, -1.499999999999999778 ) ) ;
#6728=ORIENTED_EDGE ( 'NONE', *, *, #9989, .T. ) ;
#6730=LINE ( 'NONE', #6423, #7211 ) ;
#6738=CIRCLE ( 'NONE', #6239, 2.000000000000000000 ) ;
#6744=DIRECTION ( 'NONE',  ( 0.000000000000000000, 0.000000000000000000, -1.000000000000000000 ) ) ;
#6763=VECTOR ( 'NONE', #9339, 1000.000000000000000 ) ;
#6792=ORIENTED_EDGE ( 'NONE', *, *, #2974, .T. ) ;
#6819=VERTEX_POINT ( 'NONE', #13663 ) ;
#6835=VERTEX_POINT ( 'NONE', #3064 ) ;
#6849=LINE ( 'NONE', #3523, #8929 ) ;
#6867=ORIENTED_EDGE ( 'NONE', *, *, #14255, .T. ) ;
#6944=ORIENTED_EDGE ( 'NONE', *, *, #5263, .T. ) ;
#6950=DIRECTION ( 'NONE',  ( 1.000000000000000000, 0.000000000000000000, 0.000000000000000000 ) ) ;
#6957=LINE ( 'NONE', #4643, #12631 ) ;
#6961=ADVANCED_FACE ( 'NONE', ( #8074 ), #1353, .T. ) ;
#7003=LINE ( 'NONE', #6068, #10716 ) ;
#7081=CARTESIAN_POINT ( 'NONE',  ( 4.286263797015736595E-16, 5.000000000000000000, 3.500000000000000000 ) ) ;
#7123=ORIENTED_EDGE ( 'NONE', *, *, #4389, .T. ) ;
#7146=PLANE ( 'NONE',  #4716 ) ;
#7158=ORIENTED_EDGE ( 'NONE', *, *, #13203, .F. ) ;
#7191=EDGE_CURVE ( 'NONE', #11845, #13038, #6136, .T. ) ;
#7211=VECTOR ( 'NONE', #13479, 1000.000000000000000 ) ;
#7242=DIRECTION ( 'NONE',  ( 1.000000000000000000, 0.000000000000000000, 0.000000000000000000 ) ) ;
#7263=DIRECTION ( 'NONE',  ( 0.000000000000000000, -0.000000000000000000, 1.000000000000000000 ) ) ;
#7281=( NAMED_UNIT ( * ) SI_UNIT ( $, .STERADIAN. ) SOLID_ANGLE_UNIT ( ) );
#7289=VERTEX_POINT ( 'NONE', #9850 ) ;
#7372=ORIENTED_EDGE ( 'NONE', *, *, #6458, .T. ) ;
#7394=ORIENTED_EDGE ( 'NONE', *, *, #2891, .F. ) ;
#7400=DIRECTION ( 'NONE',  ( -0.000000000000000000, 0.000000000000000000, 1.000000000000000000 ) ) ;
#7422=VERTEX_POINT ( 'NONE', #5363 ) ;
#7439=CARTESIAN_POINT ( 'NONE',  ( 0.2499999999999999445, 5.000000000000000000, -1.499999999999999778 ) ) ;
#7440=MANIFOLD_SOLID_BREP ( 'Cortar-Extruir1', #2392 ) ;
#7451=VERTEX_POINT ( 'NONE', #11756 ) ;
#7466=ORIENTED_EDGE ( 'NONE', *, *, #1683, .F. ) ;
#7469=ORIENTED_EDGE ( 'NONE', *, *, #6584, .T. ) ;
#7479=APPLICATION_CONTEXT ( 'configuration controlled 3d designs of mechanical parts and assemblies' ) ;
#7502=ORIENTED_EDGE ( 'NONE', *, *, #1400, .F. ) ;
#7627=EDGE_CURVE ( 'NONE', #6503, #10346, #6730, .T. ) ;
#7629=DIRECTION ( 'NONE',  ( -0.000000000000000000, -1.000000000000000000, -0.000000000000000000 ) ) ;
#7646=VECTOR ( 'NONE', #13717, 1000.000000000000000 ) ;
#7744=LINE ( 'NONE', #14954, #13112 ) ;
#7830=ORIENTED_EDGE ( 'NONE', *, *, #3869, .F. ) ;
#7912=AXIS2_PLACEMENT_3D ( 'NONE', #589, #8999, #9076 ) ;
#7924=EDGE_LOOP ( 'NONE', ( #2092, #1123 ) ) ;
#7930=CARTESIAN_POINT ( 'NONE',  ( 1.500000000000000000, 4.500000000000000888, -0.2499999999999997780 ) ) ;
#7939=ORIENTED_EDGE ( 'NONE', *, *, #11781, .F. ) ;
#7960=LINE ( 'NONE', #2096, #3806 ) ;
#7964=CARTESIAN_POINT ( 'NONE',  ( 0.000000000000000000, 4.000000000000000000, -2.000000000000000000 ) ) ;
#8056=ADVANCED_FACE ( 'NONE', ( #2949 ), #1790, .T. ) ;
#8074=FACE_OUTER_BOUND ( 'NONE', #11850, .T. ) ;
#8077=EDGE_LOOP ( 'NONE', ( #3884, #901, #10381, #2360 ) ) ;
#8112=DIRECTION ( 'NONE',  ( 0.000000000000000000, -1.000000000000000000, 0.000000000000000000 ) ) ;
#8120=LINE ( 'NONE', #4503, #4949 ) ;
#8143=ORIENTED_EDGE ( 'NONE', *, *, #1488, .T. ) ;
#8161=VECTOR ( 'NONE', #4198, 1000.000000000000000 ) ;
#8211=CARTESIAN_POINT ( 'NONE',  ( 0.000000000000000000, 4.000000000000000000, 0.000000000000000000 ) ) ;
#8244=ADVANCED_FACE ( 'NONE', ( #14624 ), #5252, .T. ) ;
#8252=DIRECTION ( 'NONE',  ( 0.000000000000000000, 0.000000000000000000, -1.000000000000000000 ) ) ;
#8285=CARTESIAN_POINT ( 'NONE',  ( 0.2499999999999999445, 4.500000000000000888, 1.500000000000000222 ) ) ;
#8291=CARTESIAN_POINT ( 'NONE',  ( -1.500000000000000000, 4.500000000000000888, 0.2500000000000002220 ) ) ;
#8311=VECTOR ( 'NONE', #8689, 1000.000000000000000 ) ;
#8361=CARTESIAN_POINT ( 'NONE',  ( 1.500000000000000000, 5.000000000000000000, 0.2500000000000002220 ) ) ;
#8379=AXIS2_PLACEMENT_3D ( 'NONE', #15049, #14030, #11403 ) ;
#8386=ORIENTED_EDGE ( 'NONE', *, *, #12239, .T. ) ;
#8405=VECTOR ( 'NONE', #5848, 1000.000000000000000 ) ;
#8451=DIRECTION ( 'NONE',  ( 0.000000000000000000, 0.000000000000000000, -1.000000000000000000 ) ) ;
#8470=AXIS2_PLACEMENT_3D ( 'NONE', #3580, #9762, #11831 ) ;
#8491=FACE_OUTER_BOUND ( 'NONE', #1585, .T. ) ;
#8505=EDGE_LOOP ( 'NONE', ( #13837, #13132, #13004, #2341 ) ) ;
#8613=FACE_OUTER_BOUND ( 'NONE', #5433, .T. ) ;
#8626=DIRECTION ( 'NONE',  ( 1.000000000000000000, 0.000000000000000000, 0.000000000000000000 ) ) ;
#8689=DIRECTION ( 'NONE',  ( 0.000000000000000000, 0.000000000000000000, -1.000000000000000000 ) ) ;
#8719=CIRCLE ( 'NONE', #14675, 2.000000000000000000 ) ;
#8751=ORIENTED_EDGE ( 'NONE', *, *, #14614, .F. ) ;
#8757=LINE ( 'NONE', #5423, #14102 ) ;
#8765=CARTESIAN_POINT ( 'NONE',  ( -0.2500000000000000555, 4.500000000000000888, 1.500000000000000222 ) ) ;
#8789=CARTESIAN_POINT ( 'NONE',  ( 0.000000000000000000, 4.000000000000000000, 0.000000000000000000 ) ) ;
#8800=CARTESIAN_POINT ( 'NONE',  ( -1.500000000000000000, 4.500000000000000888, -0.2499999999999997780 ) ) ;
#8828=LINE ( 'NONE', #14956, #8161 ) ;
#8847=CARTESIAN_POINT ( 'NONE',  ( -0.2500000000000000555, 4.500000000000000888, -0.2499999999999997780 ) ) ;
#8852=EDGE_CURVE ( 'NONE', #14170, #14051, #6738, .T. ) ;
#8869=CYLINDRICAL_SURFACE ( 'NONE', #4466, 3.500000000000000000 ) ;
#8910=LINE ( 'NONE', #3040, #4083 ) ;
#8929=VECTOR ( 'NONE', #3302, 1000.000000000000000 ) ;
#8939=PRODUCT_DEFINITION_FORMATION_WITH_SPECIFIED_SOURCE ( 'ANY', '', #3617, .NOT_KNOWN. ) ;
#8947=CARTESIAN_POINT ( 'NONE',  ( 0.000000000000000000, 5.000000000000000000, 0.000000000000000000 ) ) ;
#8960=CARTESIAN_POINT ( 'NONE',  ( -1.500000000000000000, 5.000000000000000000, -0.2499999999999997780 ) ) ;
#8969=EDGE_LOOP ( 'NONE', ( #11518, #9617, #15280, #8143 ) ) ;
#8974=CARTESIAN_POINT ( 'NONE',  ( 0.000000000000000000, 5.000000000000000000, 0.000000000000000000 ) ) ;
#8985=LINE ( 'NONE', #4425, #372 ) ;
#8987=AXIS2_PLACEMENT_3D ( 'NONE', #2469, #6014, #3628 ) ;
#8999=DIRECTION ( 'NONE',  ( -0.000000000000000000, 0.000000000000000000, 1.000000000000000000 ) ) ;
#9024=VERTEX_POINT ( 'NONE', #7930 ) ;
#9076=DIRECTION ( 'NONE',  ( 1.000000000000000000, 0.000000000000000000, 0.000000000000000000 ) ) ;
#9089=ORIENTED_EDGE ( 'NONE', *, *, #4243, .T. ) ;
#9116=ORIENTED_EDGE ( 'NONE', *, *, #13203, .T. ) ;
#9158=VERTEX_POINT ( 'NONE', #5761 ) ;
#9163=ORIENTED_EDGE ( 'NONE', *, *, #14614, .T. ) ;
#9203=FACE_OUTER_BOUND ( 'NONE', #8969, .T. ) ;
#9214=ORIENTED_EDGE ( 'NONE', *, *, #2692, .T. ) ;
#9226=DIRECTION ( 'NONE',  ( 0.000000000000000000, 0.000000000000000000, 1.000000000000000000 ) ) ;
#9238=ADVANCED_FACE ( 'NONE', ( #3104, #12088 ), #2673, .T. ) ;
#9258=PRODUCT_DEFINITION ( 'UNKNOWN', '', #8939, #14716 ) ;
#9296=ORIENTED_EDGE ( 'NONE', *, *, #9989, .F. ) ;
#9339=DIRECTION ( 'NONE',  ( -0.000000000000000000, -1.000000000000000000, -0.000000000000000000 ) ) ;
#9367=ORIENTED_EDGE ( 'NONE', *, *, #2974, .F. ) ;
#9371=CARTESIAN_POINT ( 'NONE',  ( 1.500000000000000000, 4.500000000000000888, 0.2500000000000002220 ) ) ;
#9380=DIRECTION ( 'NONE',  ( 0.000000000000000000, 0.000000000000000000, -1.000000000000000000 ) ) ;
#9419=AXIS2_PLACEMENT_3D ( 'NONE', #15272, #9226, #12943 ) ;
#9449=ORIENTED_EDGE ( 'NONE', *, *, #4389, .F. ) ;
#9476=LINE ( 'NONE', #11860, #11619 ) ;
#9514=DIRECTION ( 'NONE',  ( 0.000000000000000000, 1.000000000000000000, 0.000000000000000000 ) ) ;
#9535=DIRECTION ( 'NONE',  ( 0.000000000000000000, 0.000000000000000000, -1.000000000000000000 ) ) ;
#9537=ORIENTED_EDGE ( 'NONE', *, *, #749, .T. ) ;
#9613=EDGE_LOOP ( 'NONE', ( #5299, #2061, #9775, #5488 ) ) ;
#9617=ORIENTED_EDGE ( 'NONE', *, *, #12990, .F. ) ;
#9632=AXIS2_PLACEMENT_3D ( 'NONE', #8211, #3733, #12071 ) ;
#9654=PLANE ( 'NONE',  #8987 ) ;
#9669=CARTESIAN_POINT ( 'NONE',  ( -1.500000000000000000, 4.500000000000000888, 0.2500000000000002220 ) ) ;
#9690=EDGE_CURVE ( 'NONE', #6819, #5529, #8719, .T. ) ;
#9697=LINE ( 'NONE', #3984, #8311 ) ;
#9731=FACE_OUTER_BOUND ( 'NONE', #14739, .T. ) ;
#9762=DIRECTION ( 'NONE',  ( -0.000000000000000000, -1.000000000000000000, -0.000000000000000000 ) ) ;
#9775=ORIENTED_EDGE ( 'NONE', *, *, #12239, .F. ) ;
#9776=VERTEX_POINT ( 'NONE', #11613 ) ;
#9782=ORIENTED_EDGE ( 'NONE', *, *, #11502, .F. ) ;
#9817=ADVANCED_FACE ( 'NONE', ( #10759 ), #9834, .T. ) ;
#9834=CYLINDRICAL_SURFACE ( 'NONE', #8470, 2.000000000000000000 ) ;
#9850=CARTESIAN_POINT ( 'NONE',  ( 1.500000000000000000, 5.000000000000000000, -0.2499999999999997780 ) ) ;
#9854=ORIENTED_EDGE ( 'NONE', *, *, #14917, .F. ) ;
#9904=AXIS2_PLACEMENT_3D ( 'NONE', #9991, #12612, #2886 ) ;
#9906=CARTESIAN_POINT ( 'NONE',  ( 0.2499999999999999445, 4.500000000000000888, 1.500000000000000222 ) ) ;
#9908=VERTEX_POINT ( 'NONE', #5119 ) ;
#9989=EDGE_CURVE ( 'NONE', #2585, #9024, #6198, .T. ) ;
#9991=CARTESIAN_POINT ( 'NONE',  ( -0.2500000000000000555, 4.500000000000000888, 1.500000000000000222 ) ) ;
#10097=EDGE_CURVE ( 'NONE', #10548, #2585, #13630, .T. ) ;
#10142=VECTOR ( 'NONE', #14426, 1000.000000000000000 ) ;
#10223=DIRECTION ( 'NONE',  ( 1.000000000000000000, 0.000000000000000000, 0.000000000000000000 ) ) ;
#10227=CARTESIAN_POINT ( 'NONE',  ( 1.500000000000000000, 4.500000000000000888, 0.2500000000000002220 ) ) ;
#10261=ORIENTED_EDGE ( 'NONE', *, *, #14749, .F. ) ;
#10267=LINE ( 'NONE', #11203, #13612 ) ;
#10290=FACE_OUTER_BOUND ( 'NONE', #1486, .T. ) ;
#10298=EDGE_LOOP ( 'NONE', ( #13665, #14492, #11178, #15227 ) ) ;
#10326=CARTESIAN_POINT ( 'NONE',  ( -0.2500000000000000555, 4.500000000000000888, 0.2500000000000002220 ) ) ;
#10340=APPLICATION_CONTEXT ( 'configuration controlled 3d designs of mechanical parts and assemblies' ) ;
#10346=VERTEX_POINT ( 'NONE', #5639 ) ;
#10372=CIRCLE ( 'NONE', #259, 2.000000000000000000 ) ;
#10381=ORIENTED_EDGE ( 'NONE', *, *, #7191, .T. ) ;
#10422=LINE ( 'NONE', #3459, #8405 ) ;
#10438=EDGE_CURVE ( 'NONE', #14605, #4391, #7960, .T. ) ;
#10455=VECTOR ( 'NONE', #3102, 1000.000000000000000 ) ;
#10486=EDGE_CURVE ( 'NONE', #9776, #14605, #13928, .T. ) ;
#10506=ORIENTED_EDGE ( 'NONE', *, *, #45, .T. ) ;
#10519=DIRECTION ( 'NONE',  ( 1.000000000000000000, 0.000000000000000000, 0.000000000000000000 ) ) ;
#10529=ORIENTED_EDGE ( 'NONE', *, *, #1488, .F. ) ;
#10544=ADVANCED_FACE ( 'NONE', ( #8491 ), #9654, .F. ) ;
#10548=VERTEX_POINT ( 'NONE', #12126 ) ;
#10634=VECTOR ( 'NONE', #13496, 1000.000000000000000 ) ;
#10675=DIRECTION ( 'NONE',  ( -0.000000000000000000, 0.000000000000000000, 1.000000000000000000 ) ) ;
#10677=VERTEX_POINT ( 'NONE', #11810 ) ;
#10708=DIRECTION ( 'NONE',  ( -0.000000000000000000, 1.000000000000000000, -0.000000000000000000 ) ) ;
#10716=VECTOR ( 'NONE', #14128, 1000.000000000000000 ) ;
#10752=ORIENTED_EDGE ( 'NONE', *, *, #4243, .F. ) ;
#10759=FACE_OUTER_BOUND ( 'NONE', #15150, .T. ) ;
#10800=EDGE_LOOP ( 'NONE', ( #6867, #10506, #13865, #1271 ) ) ;
#10831=EDGE_LOOP ( 'NONE', ( #3823, #727, #13866, #9854 ) ) ;
#10843=CARTESIAN_POINT ( 'NONE',  ( 4.286263797015736595E-16, 5.000000000000000000, 3.500000000000000000 ) ) ;
#10869=AXIS2_PLACEMENT_3D ( 'NONE', #9371, #1341, #13085 ) ;
#10881=ORIENTED_EDGE ( 'NONE', *, *, #12073, .T. ) ;
#10914=DIRECTION ( 'NONE',  ( 1.000000000000000000, 0.000000000000000000, 0.000000000000000000 ) ) ;
#10929=LINE ( 'NONE', #6440, #13103 ) ;
#10955=AXIS2_PLACEMENT_3D ( 'NONE', #8974, #1513, #6224 ) ;
#11018=ORIENTED_EDGE ( 'NONE', *, *, #12013, .F. ) ;
#11022=PLANE ( 'NONE',  #11365 ) ;
#11089=DIRECTION ( 'NONE',  ( 0.000000000000000000, 0.000000000000000000, -1.000000000000000000 ) ) ;
#11109=FACE_OUTER_BOUND ( 'NONE', #12640, .T. ) ;
#11151=DIRECTION ( 'NONE',  ( 0.000000000000000000, 0.000000000000000000, 1.000000000000000000 ) ) ;
#11178=ORIENTED_EDGE ( 'NONE', *, *, #12261, .T. ) ;
#11194=VECTOR ( 'NONE', #8451, 1000.000000000000000 ) ;
#11203=CARTESIAN_POINT ( 'NONE',  ( 0.2499999999999999445, 4.500000000000000888, 1.500000000000000222 ) ) ;
#11220=CIRCLE ( 'NONE', #4556, 3.500000000000000000 ) ;
#11351=LINE ( 'NONE', #8960, #5765 ) ;
#11365=AXIS2_PLACEMENT_3D ( 'NONE', #14751, #6378, #12255 ) ;
#11367=VECTOR ( 'NONE', #3857, 1000.000000000000000 ) ;
#11403=DIRECTION ( 'NONE',  ( 0.000000000000000000, 0.000000000000000000, -1.000000000000000000 ) ) ;
#11502=EDGE_CURVE ( 'NONE', #3391, #12700, #7003, .T. ) ;
#11518=ORIENTED_EDGE ( 'NONE', *, *, #11502, .T. ) ;
#11613=CARTESIAN_POINT ( 'NONE',  ( -0.2500000000000000555, 4.500000000000000888, -1.499999999999999778 ) ) ;
#11619=VECTOR ( 'NONE', #14202, 1000.000000000000000 ) ;
#11632=DIRECTION ( 'NONE',  ( 0.000000000000000000, 0.000000000000000000, -1.000000000000000000 ) ) ;
#11669=CARTESIAN_POINT ( 'NONE',  ( -0.2500000000000000555, 4.500000000000000888, -1.499999999999999778 ) ) ;
#11683=DIRECTION ( 'NONE',  ( 1.000000000000000000, 0.000000000000000000, 0.000000000000000000 ) ) ;
#11700=LINE ( 'NONE', #8361, #3315 ) ;
#11756=CARTESIAN_POINT ( 'NONE',  ( 0.2499999999999999445, 5.000000000000000000, 1.500000000000000222 ) ) ;
#11775=ORIENTED_EDGE ( 'NONE', *, *, #1113, .F. ) ;
#11781=EDGE_CURVE ( 'NONE', #15055, #7289, #11700, .T. ) ;
#11805=AXIS2_PLACEMENT_3D ( 'NONE', #1397, #9514, #2480 ) ;
#11810=CARTESIAN_POINT ( 'NONE',  ( -1.500000000000000000, 5.000000000000000000, -0.2499999999999997780 ) ) ;
#11831=DIRECTION ( 'NONE',  ( 0.000000000000000000, 0.000000000000000000, -1.000000000000000000 ) ) ;
#11845=VERTEX_POINT ( 'NONE', #8291 ) ;
#11850=EDGE_LOOP ( 'NONE', ( #11018, #5383, #3881, #4653 ) ) ;
#11856=VECTOR ( 'NONE', #8252, 1000.000000000000000 ) ;
#11860=CARTESIAN_POINT ( 'NONE',  ( -0.2500000000000000555, 4.500000000000000888, 1.500000000000000222 ) ) ;
#11864=VECTOR ( 'NONE', #1350, 1000.000000000000000 ) ;
#11870=CARTESIAN_POINT ( 'NONE',  ( -0.2500000000000000555, 4.500000000000000888, 1.500000000000000222 ) ) ;
#11885=VERTEX_POINT ( 'NONE', #4667 ) ;
#11925=CARTESIAN_POINT ( 'NONE',  ( 0.000000000000000000, 4.000000000000000000, 0.000000000000000000 ) ) ;
#11981=DIRECTION ( 'NONE',  ( 1.000000000000000000, 0.000000000000000000, 0.000000000000000000 ) ) ;
#11982=ORIENTED_EDGE ( 'NONE', *, *, #15009, .F. ) ;
#12001=DIRECTION ( 'NONE',  ( -0.000000000000000000, -1.000000000000000000, -0.000000000000000000 ) ) ;
#12013=EDGE_CURVE ( 'NONE', #1308, #9158, #11220, .T. ) ;
#12030=EDGE_CURVE ( 'NONE', #1308, #6835, #6128, .T. ) ;
#12071=DIRECTION ( 'NONE',  ( 0.000000000000000000, 0.000000000000000000, 1.000000000000000000 ) ) ;
#12073=EDGE_CURVE ( 'NONE', #6503, #10677, #8985, .T. ) ;
#12088=FACE_BOUND ( 'NONE', #3967, .T. ) ;
#12125=DIRECTION ( 'NONE',  ( 1.000000000000000000, 0.000000000000000000, 0.000000000000000000 ) ) ;
#12126=CARTESIAN_POINT ( 'NONE',  ( 0.2499999999999999445, 5.000000000000000000, -0.2499999999999997780 ) ) ;
#12182=ORIENTED_EDGE ( 'NONE', *, *, #14749, .T. ) ;
#12239=EDGE_CURVE ( 'NONE', #9908, #9024, #13638, .T. ) ;
#12251=ORIENTED_EDGE ( 'NONE', *, *, #2891, .T. ) ;
#12254=DIRECTION ( 'NONE',  ( 1.000000000000000000, 0.000000000000000000, 0.000000000000000000 ) ) ;
#12255=DIRECTION ( 'NONE',  ( 0.000000000000000000, -0.000000000000000000, 1.000000000000000000 ) ) ;
#12261=EDGE_CURVE ( 'NONE', #11845, #6503, #8910, .T. ) ;
#12296=ORIENTED_EDGE ( 'NONE', *, *, #14787, .F. ) ;
#12334=AXIS2_PLACEMENT_3D ( 'NONE', #9669, #10675, #11683 ) ;
#12365=CARTESIAN_POINT ( 'NONE',  ( 0.000000000000000000, 4.000000000000000000, -3.500000000000000000 ) ) ;
#12389=CARTESIAN_POINT ( 'NONE',  ( -0.2500000000000000555, 5.000000000000000000, 1.500000000000000222 ) ) ;
#12466=DIRECTION ( 'NONE',  ( -0.000000000000000000, 1.000000000000000000, -0.000000000000000000 ) ) ;
#12477=SHAPE_REPRESENTATION ( 'BladeScrew_Predeterminado', ( #9419 ), #6228 ) ;
#12508=AXIS2_PLACEMENT_3D ( 'NONE', #4871, #14479, #7263 ) ;
#12510=DIRECTION ( 'NONE',  ( 0.000000000000000000, 0.000000000000000000, -1.000000000000000000 ) ) ;
#12511=ORIENTED_EDGE ( 'NONE', *, *, #6406, .F. ) ;
#12524=CARTESIAN_POINT ( 'NONE',  ( -1.500000000000000000, 4.500000000000000888, 0.2500000000000002220 ) ) ;
#12554=PLANE ( 'NONE',  #7912 ) ;
#12563=EDGE_LOOP ( 'NONE', ( #7502, #6944, #4602, #6356, #8386, #9296, #4999, #3662, #14196, #11982, #2466, #13615 ) ) ;
#12612=DIRECTION ( 'NONE',  ( -0.000000000000000000, 0.000000000000000000, 1.000000000000000000 ) ) ;
#12613=VECTOR ( 'NONE', #14696, 1000.000000000000000 ) ;
#12631=VECTOR ( 'NONE', #2, 1000.000000000000000 ) ;
#12640=EDGE_LOOP ( 'NONE', ( #5607, #12511, #7469, #9089 ) ) ;
#12669=VECTOR ( 'NONE', #10914, 1000.000000000000000 ) ;
#12680=DIRECTION ( 'NONE',  ( -0.000000000000000000, 1.000000000000000000, -0.000000000000000000 ) ) ;
#12700=VERTEX_POINT ( 'NONE', #4600 ) ;
#12802=EDGE_CURVE ( 'NONE', #5040, #7422, #1725, .T. ) ;
#12832=DIRECTION ( 'NONE',  ( 0.000000000000000000, 0.000000000000000000, -1.000000000000000000 ) ) ;
#12842=PLANE ( 'NONE',  #5031 ) ;
#12943=DIRECTION ( 'NONE',  ( 1.000000000000000000, 0.000000000000000000, 0.000000000000000000 ) ) ;
#12952=VERTEX_POINT ( 'NONE', #347 ) ;
#12962=DIRECTION ( 'NONE',  ( 0.000000000000000000, -1.000000000000000000, 0.000000000000000000 ) ) ;
#12990=EDGE_CURVE ( 'NONE', #5891, #12700, #10929, .T. ) ;
#13004=ORIENTED_EDGE ( 'NONE', *, *, #15009, .T. ) ;
#13016=PLANE ( 'NONE',  #10869 ) ;
#13038=VERTEX_POINT ( 'NONE', #13716 ) ;
#13085=DIRECTION ( 'NONE',  ( 0.000000000000000000, 0.000000000000000000, -1.000000000000000000 ) ) ;
#13096=CYLINDRICAL_SURFACE ( 'NONE', #14100, 2.000000000000000000 ) ;
#13103=VECTOR ( 'NONE', #14504, 1000.000000000000000 ) ;
#13112=VECTOR ( 'NONE', #3174, 1000.000000000000000 ) ;
#13132=ORIENTED_EDGE ( 'NONE', *, *, #13576, .F. ) ;
#13203=EDGE_CURVE ( 'NONE', #3391, #15055, #8120, .T. ) ;
#13208=CARTESIAN_POINT ( 'NONE',  ( -0.2500000000000000555, 5.000000000000000000, 1.500000000000000222 ) ) ;
#13260=FACE_OUTER_BOUND ( 'NONE', #1686, .T. ) ;
#13312=ADVANCED_FACE ( 'NONE', ( #5192 ), #14558, .F. ) ;
#13316=ORIENTED_EDGE ( 'NONE', *, *, #2523, .T. ) ;
#13337=DIRECTION ( 'NONE',  ( 0.000000000000000000, 0.000000000000000000, -1.000000000000000000 ) ) ;
#13349=FACE_BOUND ( 'NONE', #14582, .T. ) ;
#13445=AXIS2_PLACEMENT_3D ( 'NONE', #1699, #4181, #472 ) ;
#13462=VECTOR ( 'NONE', #6744, 1000.000000000000000 ) ;
#13479=DIRECTION ( 'NONE',  ( 1.000000000000000000, 0.000000000000000000, 0.000000000000000000 ) ) ;
#13488=PLANE ( 'NONE',  #9904 ) ;
#13493=DIRECTION ( 'NONE',  ( 0.000000000000000000, 0.000000000000000000, 1.000000000000000000 ) ) ;
#13496=DIRECTION ( 'NONE',  ( 0.000000000000000000, 0.000000000000000000, -1.000000000000000000 ) ) ;
#13548=ORIENTED_EDGE ( 'NONE', *, *, #8852, .T. ) ;
#13576=EDGE_CURVE ( 'NONE', #13038, #10677, #14848, .T. ) ;
#13612=VECTOR ( 'NONE', #12510, 1000.000000000000000 ) ;
#13615=ORIENTED_EDGE ( 'NONE', *, *, #5993, .T. ) ;
#13630=LINE ( 'NONE', #2806, #10455 ) ;
#13638=LINE ( 'NONE', #10227, #13462 ) ;
#13649=ORIENTED_EDGE ( 'NONE', *, *, #14414, .F. ) ;
#13663=CARTESIAN_POINT ( 'NONE',  ( 2.449293598294706414E-16, 0.000000000000000000, 2.000000000000000000 ) ) ;
#13665=ORIENTED_EDGE ( 'NONE', *, *, #14917, .T. ) ;
#13688=LINE ( 'NONE', #3085, #14865 ) ;
#13708=PLANE ( 'NONE',  #4000 ) ;
#13716=CARTESIAN_POINT ( 'NONE',  ( -1.500000000000000000, 4.500000000000000888, -0.2499999999999997780 ) ) ;
#13717=DIRECTION ( 'NONE',  ( -0.000000000000000000, -1.000000000000000000, -0.000000000000000000 ) ) ;
#13724=VERTEX_POINT ( 'NONE', #14358 ) ;
#13837=ORIENTED_EDGE ( 'NONE', *, *, #14130, .F. ) ;
#13864=CARTESIAN_POINT ( 'NONE',  ( 2.449293598294706414E-16, 4.000000000000000000, 2.000000000000000000 ) ) ;
#13865=ORIENTED_EDGE ( 'NONE', *, *, #1113, .T. ) ;
#13866=ORIENTED_EDGE ( 'NONE', *, *, #1400, .T. ) ;
#13928=LINE ( 'NONE', #11669, #1836 ) ;
#13933=CARTESIAN_POINT ( 'NONE',  ( 2.449293598294706414E-16, 4.000000000000000000, 2.000000000000000000 ) ) ;
#13998=ORIENTED_EDGE ( 'NONE', *, *, #14130, .T. ) ;
#14023=ADVANCED_FACE ( 'NONE', ( #9203 ), #13708, .F. ) ;
#14030=DIRECTION ( 'NONE',  ( 1.000000000000000000, 0.000000000000000000, 0.000000000000000000 ) ) ;
#14051=VERTEX_POINT ( 'NONE', #7964 ) ;
#14064=DIRECTION ( 'NONE',  ( -0.000000000000000000, 1.000000000000000000, -0.000000000000000000 ) ) ;
#14087=CIRCLE ( 'NONE', #9632, 3.500000000000000000 ) ;
#14090=AXIS2_PLACEMENT_3D ( 'NONE', #4927, #2541, #7242 ) ;
#14100=AXIS2_PLACEMENT_3D ( 'NONE', #11925, #12001, #9380 ) ;
#14102=VECTOR ( 'NONE', #10223, 1000.000000000000000 ) ;
#14128=DIRECTION ( 'NONE',  ( 0.000000000000000000, -1.000000000000000000, 0.000000000000000000 ) ) ;
#14130=EDGE_CURVE ( 'NONE', #10677, #12952, #7744, .T. ) ;
#14143=ORIENTED_EDGE ( 'NONE', *, *, #8852, .F. ) ;
#14170=VERTEX_POINT ( 'NONE', #13933 ) ;
#14188=EDGE_CURVE ( 'NONE', #7422, #10346, #6957, .T. ) ;
#14196=ORIENTED_EDGE ( 'NONE', *, *, #45, .F. ) ;
#14202=DIRECTION ( 'NONE',  ( 1.000000000000000000, 0.000000000000000000, 0.000000000000000000 ) ) ;
#14205=EDGE_LOOP ( 'NONE', ( #12182, #7830, #6598, #1348 ) ) ;
#14249=ADVANCED_BREP_SHAPE_REPRESENTATION ( '', ( #7440, #9419 ), #6228 ) ;
#14255=EDGE_CURVE ( 'NONE', #12952, #5739, #4866, .T. ) ;
#14313=FACE_OUTER_BOUND ( 'NONE', #10298, .T. ) ;
#14332=( NAMED_UNIT ( * ) PLANE_ANGLE_UNIT ( ) SI_UNIT ( $, .RADIAN. ) );
#14358=CARTESIAN_POINT ( 'NONE',  ( -0.2500000000000000555, 5.000000000000000000, -1.499999999999999778 ) ) ;
#14401=PLANE ( 'NONE',  #12334 ) ;
#14414=EDGE_CURVE ( 'NONE', #9908, #15055, #13688, .T. ) ;
#14426=DIRECTION ( 'NONE',  ( -0.000000000000000000, 1.000000000000000000, -0.000000000000000000 ) ) ;
#14428=CARTESIAN_POINT ( 'NONE',  ( 0.2499999999999999445, 4.500000000000000888, -0.2499999999999997780 ) ) ;
#14461=CARTESIAN_POINT ( 'NONE',  ( -0.2500000000000000555, 4.500000000000000888, 1.500000000000000222 ) ) ;
#14479=DIRECTION ( 'NONE',  ( -0.000000000000000000, 1.000000000000000000, 0.000000000000000000 ) ) ;
#14492=ORIENTED_EDGE ( 'NONE', *, *, #5993, .F. ) ;
#14504=DIRECTION ( 'NONE',  ( 0.000000000000000000, 0.000000000000000000, -1.000000000000000000 ) ) ;
#14558=PLANE ( 'NONE',  #3711 ) ;
#14582=EDGE_LOOP ( 'NONE', ( #9537, #13548 ) ) ;
#14605=VERTEX_POINT ( 'NONE', #5703 ) ;
#14614=EDGE_CURVE ( 'NONE', #14051, #5529, #10422, .T. ) ;
#14624=FACE_OUTER_BOUND ( 'NONE', #521, .T. ) ;
#14633=VECTOR ( 'NONE', #12962, 1000.000000000000000 ) ;
#14659=CARTESIAN_POINT ( 'NONE',  ( 0.2499999999999999445, 5.000000000000000000, 1.500000000000000222 ) ) ;
#14675=AXIS2_PLACEMENT_3D ( 'NONE', #2346, #2269, #5880 ) ;
#14696=DIRECTION ( 'NONE',  ( -0.000000000000000000, 1.000000000000000000, -0.000000000000000000 ) ) ;
#14716=DESIGN_CONTEXT ( 'detailed design', #7479, 'design' ) ;
#14739=EDGE_LOOP ( 'NONE', ( #9116, #13649, #6274, #9782 ) ) ;
#14749=EDGE_CURVE ( 'NONE', #7422, #7451, #1609, .T. ) ;
#14751=CARTESIAN_POINT ( 'NONE',  ( 0.000000000000000000, 4.000000000000000000, 0.000000000000000000 ) ) ;
#14769=DIRECTION ( 'NONE',  ( 0.000000000000000000, 1.000000000000000000, 0.000000000000000000 ) ) ;
#14775=CARTESIAN_POINT ( 'NONE',  ( -0.2500000000000000555, 4.500000000000000888, -1.499999999999999778 ) ) ;
#14787=EDGE_CURVE ( 'NONE', #13724, #4391, #3683, .T. ) ;
#14848=LINE ( 'NONE', #8800, #12613 ) ;
#14865=VECTOR ( 'NONE', #5482, 1000.000000000000000 ) ;
#14917=EDGE_CURVE ( 'NONE', #10346, #11885, #5767, .T. ) ;
#14954=CARTESIAN_POINT ( 'NONE',  ( -1.500000000000000000, 5.000000000000000000, -0.2499999999999997780 ) ) ;
#14956=CARTESIAN_POINT ( 'NONE',  ( -1.500000000000000000, 4.500000000000000888, 0.2500000000000002220 ) ) ;
#15007=LINE ( 'NONE', #6722, #1729 ) ;
#15009=EDGE_CURVE ( 'NONE', #13038, #5739, #6849, .T. ) ;
#15049=CARTESIAN_POINT ( 'NONE',  ( -0.2500000000000000555, 4.500000000000000888, 1.500000000000000222 ) ) ;
#15055=VERTEX_POINT ( 'NONE', #5837 ) ;
#15147=AXIS2_PLACEMENT_3D ( 'NONE', #12524, #6950, #12832 ) ;
#15150=EDGE_LOOP ( 'NONE', ( #9367, #1330, #9163, #7123 ) ) ;
#15160=CARTESIAN_POINT ( 'NONE',  ( 0.000000000000000000, 5.000000000000000000, -3.500000000000000000 ) ) ;
#15227=ORIENTED_EDGE ( 'NONE', *, *, #7627, .T. ) ;
#15237=LINE ( 'NONE', #15160, #6763 ) ;
#15272=CARTESIAN_POINT ( 'NONE',  ( 0.000000000000000000, 0.000000000000000000, 0.000000000000000000 ) ) ;
#15280=ORIENTED_EDGE ( 'NONE', *, *, #3869, .T. ) ;
#15346=COLOUR_RGB('Slate Gray', 0.72549020, 0.75294118, 0.79215686);
#15347=FILL_AREA_STYLE_COLOUR('',#15346);
#15348=FILL_AREA_STYLE('',(#15347));
#15349=SURFACE_STYLE_FILL_AREA(#15348);
#15350=SURFACE_SIDE_STYLE('',(#15349));
#15351=SURFACE_STYLE_USAGE(.BOTH.,#15350);
#15352=PRESENTATION_STYLE_ASSIGNMENT((#15351));
#15381=STYLED_ITEM('',(#15352),#7440);
#15382=MECHANICAL_DESIGN_GEOMETRIC_PRESENTATION_REPRESENTATION('',(#15381),#6228);
ENDSEC;
END-ISO-10303-21;
